ISO-10303-21;
HEADER;
/* Generated by software containing ST-Developer
 * from STEP Tools, Inc. (www.steptools.com) 
 */
/* OPTION: using custom renumber hook */

FILE_DESCRIPTION(
/* description */ ('STEP AP242 Edition 2', 'CAx-IF Rec.Pracs.---Representation and Presentation of Product Manufa
cturing Information (PMI)---4.0---2014-10-13', 'CAx-IF Rec.Pracs.---3D Tessellated Geometry---0.4---2014-09-14', '2;1', 'CAx-IF Rec.Pracs.---User Defined Attributes---1.5---2016-08-15'),
/* implementation_level */ '2;1');

FILE_NAME(
/* name */ 'refill_port.step',
/* time_stamp */ '2026-10-08T12:15:07Z',
/* author */ (''),
/* organization */ (''),
/* preprocessor_version */ 'ST-DEVELOPER v20',
/* originating_system */ 'ONSHAPE BY PTC INC, 1.221',
/* authorisation */ '  ');

FILE_SCHEMA (('AP242_MANAGED_MODEL_BASED_3D_ENGINEERING_MIM_LF { 1 0 10303 442 3 1 4 }'));
ENDSEC;

DATA;
#60=COLOUR_RGB('', 0.66274510, 0.83137255, 0.94901961);
#215=SHAPE_REPRESENTATION_RELATIONSHIP('','',#13789,#242);
#242=ADVANCED_BREP_SHAPE_REPRESENTATION('',(#13733),#45479);
#755=CIRCLE('',#14662,0.000477030566374308);
#756=CIRCLE('',#14663,0.00322703056637436);
#757=CIRCLE('',#14664,0.000477030566374308);
#758=CIRCLE('',#14665,0.00227296943362574);
#759=CIRCLE('',#14667,0.000477030566374308);
#760=CIRCLE('',#14669,0.000477030566374308);
#761=CIRCLE('',#14671,0.000477030566374308);
#762=CIRCLE('',#14672,0.00227296943362564);
#763=CIRCLE('',#14673,0.000477030566374308);
#764=CIRCLE('',#14674,0.00322703056637426);
#765=CIRCLE('',#14676,0.00322703056637426);
#766=CIRCLE('',#14678,0.00227296943362564);
#767=CIRCLE('',#14680,0.0035);
#768=CIRCLE('',#14682,0.001);
#769=CIRCLE('',#14684,0.00322703056637436);
#770=CIRCLE('',#14685,0.00227296943362574);
#771=CIRCLE('',#14686,0.0035);
#772=CIRCLE('',#14687,0.001);
#773=CIRCLE('',#14688,0.000477030566374308);
#774=CIRCLE('',#14689,0.000477030566374308);
#1396=PLANE('',#14661);
#1397=PLANE('',#14670);
#1398=PLANE('',#14679);
#1399=PLANE('',#14681);
#1400=PLANE('',#14683);
#1693=CYLINDRICAL_SURFACE('',#14666,0.000477030566374308);
#1694=CYLINDRICAL_SURFACE('',#14668,0.000477030566374308);
#1695=CYLINDRICAL_SURFACE('',#14675,0.00322703056637436);
#1696=CYLINDRICAL_SURFACE('',#14677,0.00227296943362574);
#1697=CYLINDRICAL_SURFACE('',#14690,0.001);
#1698=CYLINDRICAL_SURFACE('',#14691,0.0035);
#1699=CYLINDRICAL_SURFACE('',#14692,0.000477030566374308);
#1700=CYLINDRICAL_SURFACE('',#14693,0.000477030566374308);
#1701=CYLINDRICAL_SURFACE('',#14694,0.00322703056637436);
#1702=CYLINDRICAL_SURFACE('',#14695,0.00227296943362574);
#4016=ORIENTED_EDGE('',*,*,#6655,.F.);
#4017=ORIENTED_EDGE('',*,*,#6656,.F.);
#4018=ORIENTED_EDGE('',*,*,#6657,.F.);
#4019=ORIENTED_EDGE('',*,*,#6658,.F.);
#4020=ORIENTED_EDGE('',*,*,#6659,.F.);
#4021=ORIENTED_EDGE('',*,*,#6660,.F.);
#4022=ORIENTED_EDGE('',*,*,#6657,.T.);
#4023=ORIENTED_EDGE('',*,*,#6661,.T.);
#4024=ORIENTED_EDGE('',*,*,#6662,.F.);
#4025=ORIENTED_EDGE('',*,*,#6663,.F.);
#4026=ORIENTED_EDGE('',*,*,#6655,.T.);
#4027=ORIENTED_EDGE('',*,*,#6664,.T.);
#4028=ORIENTED_EDGE('',*,*,#6665,.F.);
#4029=ORIENTED_EDGE('',*,*,#6666,.F.);
#4030=ORIENTED_EDGE('',*,*,#6667,.F.);
#4031=ORIENTED_EDGE('',*,*,#6668,.F.);
#4032=ORIENTED_EDGE('',*,*,#6669,.F.);
#4033=ORIENTED_EDGE('',*,*,#6670,.F.);
#4034=ORIENTED_EDGE('',*,*,#6668,.T.);
#4035=ORIENTED_EDGE('',*,*,#6671,.T.);
#4036=ORIENTED_EDGE('',*,*,#6672,.F.);
#4037=ORIENTED_EDGE('',*,*,#6673,.F.);
#4038=ORIENTED_EDGE('',*,*,#6666,.T.);
#4039=ORIENTED_EDGE('',*,*,#6674,.T.);
#4040=ORIENTED_EDGE('',*,*,#6675,.T.);
#4041=ORIENTED_EDGE('',*,*,#6676,.F.);
#4042=ORIENTED_EDGE('',*,*,#6677,.T.);
#4043=ORIENTED_EDGE('',*,*,#6662,.T.);
#4044=ORIENTED_EDGE('',*,*,#6678,.T.);
#4045=ORIENTED_EDGE('',*,*,#6659,.T.);
#4046=ORIENTED_EDGE('',*,*,#6679,.F.);
#4047=ORIENTED_EDGE('',*,*,#6680,.T.);
#4048=ORIENTED_EDGE('',*,*,#6672,.T.);
#4049=ORIENTED_EDGE('',*,*,#6681,.T.);
#4050=ORIENTED_EDGE('',*,*,#6669,.T.);
#4051=ORIENTED_EDGE('',*,*,#6682,.T.);
#4052=ORIENTED_EDGE('',*,*,#6680,.F.);
#4053=ORIENTED_EDGE('',*,*,#6676,.T.);
#4054=ORIENTED_EDGE('',*,*,#6679,.T.);
#4055=ORIENTED_EDGE('',*,*,#6675,.F.);
#4056=ORIENTED_EDGE('',*,*,#6665,.T.);
#4057=ORIENTED_EDGE('',*,*,#6670,.T.);
#4058=ORIENTED_EDGE('',*,*,#6681,.F.);
#4059=ORIENTED_EDGE('',*,*,#6674,.F.);
#4060=ORIENTED_EDGE('',*,*,#6667,.T.);
#4061=ORIENTED_EDGE('',*,*,#6673,.T.);
#4062=ORIENTED_EDGE('',*,*,#6682,.F.);
#4063=ORIENTED_EDGE('',*,*,#6671,.F.);
#4064=ORIENTED_EDGE('',*,*,#6656,.T.);
#4065=ORIENTED_EDGE('',*,*,#6663,.T.);
#4066=ORIENTED_EDGE('',*,*,#6677,.F.);
#4067=ORIENTED_EDGE('',*,*,#6661,.F.);
#4068=ORIENTED_EDGE('',*,*,#6658,.T.);
#4069=ORIENTED_EDGE('',*,*,#6660,.T.);
#4070=ORIENTED_EDGE('',*,*,#6678,.F.);
#4071=ORIENTED_EDGE('',*,*,#6664,.F.);
#6655=EDGE_CURVE('',#8192,#8193,#755,.T.);
#6656=EDGE_CURVE('',#8194,#8192,#756,.T.);
#6657=EDGE_CURVE('',#8195,#8194,#757,.T.);
#6658=EDGE_CURVE('',#8193,#8195,#758,.T.);
#6659=EDGE_CURVE('',#8196,#8197,#759,.T.);
#6660=EDGE_CURVE('',#8195,#8196,#9247,.T.);
#6661=EDGE_CURVE('',#8194,#8197,#9248,.T.);
#6662=EDGE_CURVE('',#8198,#8199,#760,.T.);
#6663=EDGE_CURVE('',#8192,#8198,#9249,.T.);
#6664=EDGE_CURVE('',#8193,#8199,#9250,.T.);
#6665=EDGE_CURVE('',#8200,#8201,#761,.T.);
#6666=EDGE_CURVE('',#8202,#8200,#762,.T.);
#6667=EDGE_CURVE('',#8203,#8202,#763,.T.);
#6668=EDGE_CURVE('',#8201,#8203,#764,.T.);
#6669=EDGE_CURVE('',#8204,#8205,#765,.T.);
#6670=EDGE_CURVE('',#8201,#8204,#9251,.T.);
#6671=EDGE_CURVE('',#8203,#8205,#9252,.T.);
#6672=EDGE_CURVE('',#8206,#8207,#766,.T.);
#6673=EDGE_CURVE('',#8202,#8206,#9253,.T.);
#6674=EDGE_CURVE('',#8200,#8207,#9254,.T.);
#6675=EDGE_CURVE('',#8208,#8208,#767,.T.);
#6676=EDGE_CURVE('',#8209,#8209,#768,.T.);
#6677=EDGE_CURVE('',#8197,#8198,#769,.T.);
#6678=EDGE_CURVE('',#8199,#8196,#770,.T.);
#6679=EDGE_CURVE('',#8210,#8210,#771,.T.);
#6680=EDGE_CURVE('',#8211,#8211,#772,.T.);
#6681=EDGE_CURVE('',#8207,#8204,#773,.T.);
#6682=EDGE_CURVE('',#8205,#8206,#774,.T.);
#8192=VERTEX_POINT('',#34985);
#8193=VERTEX_POINT('',#34986);
#8194=VERTEX_POINT('',#34988);
#8195=VERTEX_POINT('',#34990);
#8196=VERTEX_POINT('',#34994);
#8197=VERTEX_POINT('',#34995);
#8198=VERTEX_POINT('',#35000);
#8199=VERTEX_POINT('',#35001);
#8200=VERTEX_POINT('',#35006);
#8201=VERTEX_POINT('',#35007);
#8202=VERTEX_POINT('',#35009);
#8203=VERTEX_POINT('',#35011);
#8204=VERTEX_POINT('',#35015);
#8205=VERTEX_POINT('',#35016);
#8206=VERTEX_POINT('',#35021);
#8207=VERTEX_POINT('',#35022);
#8208=VERTEX_POINT('',#35027);
#8209=VERTEX_POINT('',#35030);
#8210=VERTEX_POINT('',#35035);
#8211=VERTEX_POINT('',#35037);
#9247=LINE('',#34996,#10075);
#9248=LINE('',#34997,#10076);
#9249=LINE('',#35002,#10077);
#9250=LINE('',#35003,#10078);
#9251=LINE('',#35017,#10079);
#9252=LINE('',#35018,#10080);
#9253=LINE('',#35023,#10081);
#9254=LINE('',#35024,#10082);
#10075=VECTOR('',#17501,1.);
#10076=VECTOR('',#17502,1.);
#10077=VECTOR('',#17507,1.);
#10078=VECTOR('',#17508,1.);
#10079=VECTOR('',#17523,1.);
#10080=VECTOR('',#17524,1.);
#10081=VECTOR('',#17529,1.);
#10082=VECTOR('',#17530,1.);
#11072=EDGE_LOOP('',(#4016,#4017,#4018,#4019));
#11073=EDGE_LOOP('',(#4020,#4021,#4022,#4023));
#11074=EDGE_LOOP('',(#4024,#4025,#4026,#4027));
#11075=EDGE_LOOP('',(#4028,#4029,#4030,#4031));
#11076=EDGE_LOOP('',(#4032,#4033,#4034,#4035));
#11077=EDGE_LOOP('',(#4036,#4037,#4038,#4039));
#11078=EDGE_LOOP('',(#4040));
#11079=EDGE_LOOP('',(#4041));
#11080=EDGE_LOOP('',(#4042,#4043,#4044,#4045));
#11081=EDGE_LOOP('',(#4046));
#11082=EDGE_LOOP('',(#4047));
#11083=EDGE_LOOP('',(#4048,#4049,#4050,#4051));
#11084=EDGE_LOOP('',(#4052));
#11085=EDGE_LOOP('',(#4053));
#11086=EDGE_LOOP('',(#4054));
#11087=EDGE_LOOP('',(#4055));
#11088=EDGE_LOOP('',(#4056,#4057,#4058,#4059));
#11089=EDGE_LOOP('',(#4060,#4061,#4062,#4063));
#11090=EDGE_LOOP('',(#4064,#4065,#4066,#4067));
#11091=EDGE_LOOP('',(#4068,#4069,#4070,#4071));
#12189=FACE_BOUND('',#11072,.T.);
#12190=FACE_BOUND('',#11073,.T.);
#12191=FACE_BOUND('',#11074,.T.);
#12192=FACE_BOUND('',#11075,.T.);
#12193=FACE_BOUND('',#11076,.T.);
#12194=FACE_BOUND('',#11077,.T.);
#12195=FACE_BOUND('',#11078,.T.);
#12196=FACE_BOUND('',#11079,.T.);
#12197=FACE_BOUND('',#11080,.T.);
#12198=FACE_BOUND('',#11081,.T.);
#12199=FACE_BOUND('',#11082,.T.);
#12200=FACE_BOUND('',#11083,.T.);
#12201=FACE_BOUND('',#11084,.T.);
#12202=FACE_BOUND('',#11085,.T.);
#12203=FACE_BOUND('',#11086,.T.);
#12204=FACE_BOUND('',#11087,.T.);
#12205=FACE_BOUND('',#11088,.T.);
#12206=FACE_BOUND('',#11089,.T.);
#12207=FACE_BOUND('',#11090,.T.);
#12208=FACE_BOUND('',#11091,.T.);
#13167=ADVANCED_FACE('',(#12189),#1396,.T.);
#13168=ADVANCED_FACE('',(#12190),#1693,.T.);
#13169=ADVANCED_FACE('',(#12191),#1694,.T.);
#13170=ADVANCED_FACE('',(#12192),#1397,.T.);
#13171=ADVANCED_FACE('',(#12193),#1695,.T.);
#13172=ADVANCED_FACE('',(#12194),#1696,.F.);
#13173=ADVANCED_FACE('',(#12195),#1398,.T.);
#13174=ADVANCED_FACE('',(#12196),#1399,.F.);
#13175=ADVANCED_FACE('',(#12197,#12198,#12199,#12200),#1400,.F.);
#13176=ADVANCED_FACE('',(#12201,#12202),#1697,.T.);
#13177=ADVANCED_FACE('',(#12203,#12204),#1698,.T.);
#13178=ADVANCED_FACE('',(#12205),#1699,.T.);
#13179=ADVANCED_FACE('',(#12206),#1700,.T.);
#13180=ADVANCED_FACE('',(#12207),#1701,.T.);
#13181=ADVANCED_FACE('',(#12208),#1702,.F.);
#13516=CLOSED_SHELL('',(#13167,#13168,#13169,#13170,#13171,#13172,#13173,
#13174,#13175,#13176,#13177,#13178,#13179,#13180,#13181));
#13543=STYLED_ITEM('',(#13570),#13733);
#13570=PRESENTATION_STYLE_ASSIGNMENT((#13597));
#13597=SURFACE_STYLE_USAGE(.BOTH.,#13624);
#13624=SURFACE_SIDE_STYLE('',(#13651));
#13651=SURFACE_STYLE_FILL_AREA(#13678);
#13678=FILL_AREA_STYLE('',(#13705));
#13705=FILL_AREA_STYLE_COLOUR('',#60);
#13733=MANIFOLD_SOLID_BREP('refill_port',#13516);
#13761=SHAPE_DEFINITION_REPRESENTATION(#45555,#13789);
#13789=SHAPE_REPRESENTATION('refill_port',(#13802),#45479);
#13802=AXIS2_PLACEMENT_3D('',#19109,#15295,#15296);
#14661=AXIS2_PLACEMENT_3D('',#34983,#17487,#17488);
#14662=AXIS2_PLACEMENT_3D('',#34984,#17489,#17490);
#14663=AXIS2_PLACEMENT_3D('',#34987,#17491,#17492);
#14664=AXIS2_PLACEMENT_3D('',#34989,#17493,#17494);
#14665=AXIS2_PLACEMENT_3D('',#34991,#17495,#17496);
#14666=AXIS2_PLACEMENT_3D('',#34992,#17497,#17498);
#14667=AXIS2_PLACEMENT_3D('',#34993,#17499,#17500);
#14668=AXIS2_PLACEMENT_3D('',#34998,#17503,#17504);
#14669=AXIS2_PLACEMENT_3D('',#34999,#17505,#17506);
#14670=AXIS2_PLACEMENT_3D('',#35004,#17509,#17510);
#14671=AXIS2_PLACEMENT_3D('',#35005,#17511,#17512);
#14672=AXIS2_PLACEMENT_3D('',#35008,#17513,#17514);
#14673=AXIS2_PLACEMENT_3D('',#35010,#17515,#17516);
#14674=AXIS2_PLACEMENT_3D('',#35012,#17517,#17518);
#14675=AXIS2_PLACEMENT_3D('',#35013,#17519,#17520);
#14676=AXIS2_PLACEMENT_3D('',#35014,#17521,#17522);
#14677=AXIS2_PLACEMENT_3D('',#35019,#17525,#17526);
#14678=AXIS2_PLACEMENT_3D('',#35020,#17527,#17528);
#14679=AXIS2_PLACEMENT_3D('',#35025,#17531,#17532);
#14680=AXIS2_PLACEMENT_3D('',#35026,#17533,#17534);
#14681=AXIS2_PLACEMENT_3D('',#35028,#17535,#17536);
#14682=AXIS2_PLACEMENT_3D('',#35029,#17537,#17538);
#14683=AXIS2_PLACEMENT_3D('',#35031,#17539,#17540);
#14684=AXIS2_PLACEMENT_3D('',#35032,#17541,#17542);
#14685=AXIS2_PLACEMENT_3D('',#35033,#17543,#17544);
#14686=AXIS2_PLACEMENT_3D('',#35034,#17545,#17546);
#14687=AXIS2_PLACEMENT_3D('',#35036,#17547,#17548);
#14688=AXIS2_PLACEMENT_3D('',#35038,#17549,#17550);
#14689=AXIS2_PLACEMENT_3D('',#35039,#17551,#17552);
#14690=AXIS2_PLACEMENT_3D('',#35040,#17553,#17554);
#14691=AXIS2_PLACEMENT_3D('',#35041,#17555,#17556);
#14692=AXIS2_PLACEMENT_3D('',#35042,#17557,#17558);
#14693=AXIS2_PLACEMENT_3D('',#35043,#17559,#17560);
#14694=AXIS2_PLACEMENT_3D('',#35044,#17561,#17562);
#14695=AXIS2_PLACEMENT_3D('',#35045,#17563,#17564);
#15295=DIRECTION('',(0.,0.,1.));
#15296=DIRECTION('',(1.,0.,0.));
#17487=DIRECTION('',(0.,0.,1.));
#17488=DIRECTION('',(1.,0.,0.));
#17489=DIRECTION('',(0.,0.,-1.));
#17490=DIRECTION('',(1.,0.,0.));
#17491=DIRECTION('',(0.,0.,-1.));
#17492=DIRECTION('',(1.,0.,0.));
#17493=DIRECTION('',(0.,0.,-1.));
#17494=DIRECTION('',(1.,0.,0.));
#17495=DIRECTION('',(0.,0.,1.));
#17496=DIRECTION('',(1.,0.,0.));
#17497=DIRECTION('',(0.,0.,-1.));
#17498=DIRECTION('',(-1.,0.,0.));
#17499=DIRECTION('',(0.,0.,-1.));
#17500=DIRECTION('',(1.,0.,0.));
#17501=DIRECTION('',(0.,0.,-1.));
#17502=DIRECTION('',(0.,0.,-1.));
#17503=DIRECTION('',(0.,0.,-1.));
#17504=DIRECTION('',(-1.,0.,0.));
#17505=DIRECTION('',(0.,0.,-1.));
#17506=DIRECTION('',(1.,0.,0.));
#17507=DIRECTION('',(0.,0.,-1.));
#17508=DIRECTION('',(0.,0.,-1.));
#17509=DIRECTION('',(0.,0.,1.));
#17510=DIRECTION('',(1.,0.,0.));
#17511=DIRECTION('',(0.,0.,-1.));
#17512=DIRECTION('',(-1.,0.,0.));
#17513=DIRECTION('',(0.,0.,1.));
#17514=DIRECTION('',(-1.,0.,0.));
#17515=DIRECTION('',(0.,0.,-1.));
#17516=DIRECTION('',(-1.,0.,0.));
#17517=DIRECTION('',(0.,0.,-1.));
#17518=DIRECTION('',(-1.,0.,0.));
#17519=DIRECTION('',(0.,0.,-1.));
#17520=DIRECTION('',(-1.,0.,0.));
#17521=DIRECTION('',(0.,0.,-1.));
#17522=DIRECTION('',(-1.,0.,0.));
#17523=DIRECTION('',(0.,0.,-1.));
#17524=DIRECTION('',(0.,0.,-1.));
#17525=DIRECTION('',(0.,0.,-1.));
#17526=DIRECTION('',(-1.,0.,0.));
#17527=DIRECTION('',(0.,0.,1.));
#17528=DIRECTION('',(-1.,0.,0.));
#17529=DIRECTION('',(0.,0.,-1.));
#17530=DIRECTION('',(0.,0.,-1.));
#17531=DIRECTION('',(0.,0.,-1.));
#17532=DIRECTION('',(-1.,0.,0.));
#17533=DIRECTION('',(0.,0.,-1.));
#17534=DIRECTION('',(-1.,0.,0.));
#17535=DIRECTION('',(0.,0.,-1.));
#17536=DIRECTION('',(-1.,0.,0.));
#17537=DIRECTION('',(0.,0.,-1.));
#17538=DIRECTION('',(-1.,0.,0.));
#17539=DIRECTION('',(0.,0.,-1.));
#17540=DIRECTION('',(-1.,0.,0.));
#17541=DIRECTION('',(0.,0.,-1.));
#17542=DIRECTION('',(1.,0.,0.));
#17543=DIRECTION('',(0.,0.,1.));
#17544=DIRECTION('',(1.,0.,0.));
#17545=DIRECTION('',(0.,0.,-1.));
#17546=DIRECTION('',(-1.,0.,0.));
#17547=DIRECTION('',(0.,0.,-1.));
#17548=DIRECTION('',(-1.,0.,0.));
#17549=DIRECTION('',(0.,0.,-1.));
#17550=DIRECTION('',(-1.,0.,0.));
#17551=DIRECTION('',(0.,0.,-1.));
#17552=DIRECTION('',(-1.,0.,0.));
#17553=DIRECTION('',(0.,0.,-1.));
#17554=DIRECTION('',(-1.,0.,0.));
#17555=DIRECTION('',(0.,0.,1.));
#17556=DIRECTION('',(1.,0.,0.));
#17557=DIRECTION('',(0.,0.,-1.));
#17558=DIRECTION('',(-1.,0.,0.));
#17559=DIRECTION('',(0.,0.,-1.));
#17560=DIRECTION('',(-1.,0.,0.));
#17561=DIRECTION('',(0.,0.,-1.));
#17562=DIRECTION('',(-1.,0.,0.));
#17563=DIRECTION('',(0.,0.,-1.));
#17564=DIRECTION('',(-1.,0.,0.));
#19109=CARTESIAN_POINT('',(0.,0.,0.));
#34983=CARTESIAN_POINT('',(-0.012852081728299,0.0305608891324553,0.026));
#34984=CARTESIAN_POINT('',(-0.014204163456598,0.0308108891324553,0.026));
#34985=CARTESIAN_POINT('',(-0.0146732429566961,0.0308976219627052,0.026));
#34986=CARTESIAN_POINT('',(-0.0137350839565,0.0307241563022055,0.026));
#34987=CARTESIAN_POINT('',(-0.0115,0.0303108891324553,0.026));
#34988=CARTESIAN_POINT('',(-0.0146732429566961,0.0297241563022054,0.026));
#34989=CARTESIAN_POINT('',(-0.014204163456598,0.0298108891324554,0.026));
#34990=CARTESIAN_POINT('',(-0.0137350839565,0.0298976219627052,0.026));
#34991=CARTESIAN_POINT('',(-0.0115,0.0303108891324553,0.026));
#34992=CARTESIAN_POINT('',(-0.014204163456598,0.0298108891324554,0.026));
#34993=CARTESIAN_POINT('',(-0.014204163456598,0.0298108891324554,0.021));
#34994=CARTESIAN_POINT('',(-0.0137350839565,0.0298976219627052,0.021));
#34995=CARTESIAN_POINT('',(-0.0146732429566961,0.0297241563022054,0.021));
#34996=CARTESIAN_POINT('',(-0.0137350839565,0.0298976219627052,0.026));
#34997=CARTESIAN_POINT('',(-0.0146732429566961,0.0297241563022054,0.026));
#34998=CARTESIAN_POINT('',(-0.014204163456598,0.0308108891324553,0.026));
#34999=CARTESIAN_POINT('',(-0.014204163456598,0.0308108891324553,0.021));
#35000=CARTESIAN_POINT('',(-0.0146732429566961,0.0308976219627052,0.021));
#35001=CARTESIAN_POINT('',(-0.0137350839565,0.0307241563022055,0.021));
#35002=CARTESIAN_POINT('',(-0.0146732429566961,0.0308976219627052,0.026));
#35003=CARTESIAN_POINT('',(-0.0137350839565,0.0307241563022055,0.026));
#35004=CARTESIAN_POINT('',(-0.012852081728299,0.0305608891324553,0.026));
#35005=CARTESIAN_POINT('',(-0.00879583654340205,0.0308108891324553,0.026));
#35006=CARTESIAN_POINT('',(-0.0092649160435001,0.0307241563022055,0.026));
#35007=CARTESIAN_POINT('',(-0.008326757043304,0.0308976219627052,0.026));
#35008=CARTESIAN_POINT('',(-0.0115,0.0303108891324553,0.026));
#35009=CARTESIAN_POINT('',(-0.0092649160435001,0.0298976219627052,0.026));
#35010=CARTESIAN_POINT('',(-0.00879583654340205,0.0298108891324554,0.026));
#35011=CARTESIAN_POINT('',(-0.00832675704330399,0.0297241563022054,0.026));
#35012=CARTESIAN_POINT('',(-0.0115,0.0303108891324553,0.026));
#35013=CARTESIAN_POINT('',(-0.0115,0.0303108891324553,0.026));
#35014=CARTESIAN_POINT('',(-0.0115,0.0303108891324553,0.021));
#35015=CARTESIAN_POINT('',(-0.00832675704330399,0.0308976219627052,0.021));
#35016=CARTESIAN_POINT('',(-0.008326757043304,0.0297241563022054,0.021));
#35017=CARTESIAN_POINT('',(-0.008326757043304,0.0308976219627052,0.026));
#35018=CARTESIAN_POINT('',(-0.008326757043304,0.0297241563022054,0.026));
#35019=CARTESIAN_POINT('',(-0.0115,0.0303108891324553,0.026));
#35020=CARTESIAN_POINT('',(-0.0115,0.0303108891324553,0.021));
#35021=CARTESIAN_POINT('',(-0.0092649160435001,0.0298976219627052,0.021));
#35022=CARTESIAN_POINT('',(-0.0092649160435001,0.0307241563022055,0.021));
#35023=CARTESIAN_POINT('',(-0.0092649160435001,0.0298976219627052,0.026));
#35024=CARTESIAN_POINT('',(-0.0092649160435001,0.0307241563022055,0.026));
#35025=CARTESIAN_POINT('',(-0.0115,0.0303108891324553,0.018));
#35026=CARTESIAN_POINT('',(-0.0115,0.0303108891324553,0.018));
#35027=CARTESIAN_POINT('',(-0.015,0.0303108891324553,0.018));
#35028=CARTESIAN_POINT('',(0.,0.,0.025));
#35029=CARTESIAN_POINT('',(-0.0115,0.0303108891324553,0.025));
#35030=CARTESIAN_POINT('',(-0.0125,0.0303108891324553,0.025));
#35031=CARTESIAN_POINT('',(-0.0115,0.0303108891324553,0.021));
#35032=CARTESIAN_POINT('',(-0.0115,0.0303108891324553,0.021));
#35033=CARTESIAN_POINT('',(-0.0115,0.0303108891324553,0.021));
#35034=CARTESIAN_POINT('',(-0.0115,0.0303108891324553,0.021));
#35035=CARTESIAN_POINT('',(-0.015,0.0303108891324553,0.021));
#35036=CARTESIAN_POINT('',(-0.0115,0.0303108891324553,0.021));
#35037=CARTESIAN_POINT('',(-0.0125,0.0303108891324553,0.021));
#35038=CARTESIAN_POINT('',(-0.00879583654340205,0.0308108891324553,0.021));
#35039=CARTESIAN_POINT('',(-0.00879583654340205,0.0298108891324554,0.021));
#35040=CARTESIAN_POINT('',(-0.0115,0.0303108891324553,0.025));
#35041=CARTESIAN_POINT('',(-0.0115,0.0303108891324553,0.018));
#35042=CARTESIAN_POINT('',(-0.00879583654340205,0.0308108891324553,0.026));
#35043=CARTESIAN_POINT('',(-0.00879583654340205,0.0298108891324554,0.026));
#35044=CARTESIAN_POINT('',(-0.0115,0.0303108891324553,0.026));
#35045=CARTESIAN_POINT('',(-0.0115,0.0303108891324553,0.026));
#45463=MECHANICAL_DESIGN_GEOMETRIC_PRESENTATION_REPRESENTATION('',(#13543),#45464);
#45464=(
GEOMETRIC_REPRESENTATION_CONTEXT(3)
GLOBAL_UNCERTAINTY_ASSIGNED_CONTEXT((#45492))
GLOBAL_UNIT_ASSIGNED_CONTEXT((#45522,#45521,#45520))
REPRESENTATION_CONTEXT('MAS-690','TOP_LEVEL_ASSEMBLY_PART')
);
#45479=(
GEOMETRIC_REPRESENTATION_CONTEXT(3)
GLOBAL_UNCERTAINTY_ASSIGNED_CONTEXT((#45507))
GLOBAL_UNIT_ASSIGNED_CONTEXT((#45522,#45521,#45520))
REPRESENTATION_CONTEXT('refill_port','COMPONENT_PART')
);
#45492=UNCERTAINTY_MEASURE_WITH_UNIT(LENGTH_MEASURE(1.E-8),#45522,
'DISTANCE_ACCURACY_VALUE','Maximum Tolerance applied to model');
#45507=UNCERTAINTY_MEASURE_WITH_UNIT(LENGTH_MEASURE(1.E-6),#45522,
'DISTANCE_ACCURACY_VALUE','Maximum Tolerance applied to model');
#45520=(
NAMED_UNIT(*)
SI_UNIT($,.STERADIAN.)
SOLID_ANGLE_UNIT()
);
#45521=(
NAMED_UNIT(*)
PLANE_ANGLE_UNIT()
SI_UNIT($,.RADIAN.)
);
#45522=(
LENGTH_UNIT()
NAMED_UNIT(*)
SI_UNIT($,.METRE.)
);
#45555=PRODUCT_DEFINITION_SHAPE('','',#45600);
#45600=PRODUCT_DEFINITION('','',#45656,#45628);
#45628=PRODUCT_DEFINITION_CONTEXT('',#45782,'design');
#45656=PRODUCT_DEFINITION_FORMATION_WITH_SPECIFIED_SOURCE('','',#45712,
 .NOT_KNOWN.);
#45712=PRODUCT('refill_port','refill_port','refill_port',(#45768));
#45768=PRODUCT_CONTEXT('',#45782,'mechanical');
#45782=APPLICATION_CONTEXT('managed model based 3d engineering');
ENDSEC;
END-ISO-10303-21;
